ISO-10303-21;
HEADER;
FILE_DESCRIPTION (('STEP AP214'),
    '1' );
FILE_NAME ('hex screw gradeab_iso_ISO 4017 - M8 x 16-N.step',
    '2026-10-24T00:28:05',
    ( '' ),
    ( '' ),
    'SwSTEP 2.0',
    'SolidWorks 2025',
    '' );
FILE_SCHEMA (( 'AUTOMOTIVE_DESIGN' ));
ENDSEC;

DATA;
#5=FACE_BOUND ( 'NONE', #9195, .T. ) ;
#87=CARTESIAN_POINT ( 'NONE',  ( 5.299999999999999822, 7.960204194457796463E-16, -6.500000000000000888 ) ) ;
#106=CARTESIAN_POINT ( 'NONE',  ( 0.000000000000000000, -5.629165124598843661, 3.250000000000012434 ) ) ;
#130=CIRCLE ( 'NONE', #6669, 6.500000000000000888 ) ;
#145=PRODUCT_DEFINITION_CONTEXT ( 'detailed design', #14845, 'design' ) ;
#147=VECTOR ( 'NONE', #5877, 1000.000000000000000 ) ;
#151=ORIENTED_EDGE ( 'NONE', *, *, #2836, .T. ) ;
#158=CARTESIAN_POINT ( 'NONE',  ( 4.700000000000000178, 6.500000000000000888, 0.000000000000000000 ) ) ;
#171=DIRECTION ( 'NONE',  ( 1.000000000000000000, 0.000000000000000000, 0.000000000000000000 ) ) ;
#173=EDGE_CURVE ( 'NONE', #3963, #2116, #12492, .T. ) ;
#211=FACE_OUTER_BOUND ( 'NONE', #7331, .T. ) ;
#321=ORIENTED_EDGE ( 'NONE', *, *, #1301, .F. ) ;
#338=ADVANCED_FACE ( 'NONE', ( #9446 ), #11276, .T. ) ;
#340=CARTESIAN_POINT ( 'NONE',  ( -5.251604272976662102E-16, 0.6351314446054973084, -6.500000000000000000 ) ) ;
#390=( GEOMETRIC_REPRESENTATION_CONTEXT ( 3 ) GLOBAL_UNCERTAINTY_ASSIGNED_CONTEXT ( ( #21302 ) ) GLOBAL_UNIT_ASSIGNED_CONTEXT ( ( #15423, #17981, #14445 ) ) REPRESENTATION_CONTEXT ( 'NONE', 'WORKASPACE' ) );
#416=VECTOR ( 'NONE', #5059, 1000.000000000000000 ) ;
#433=CARTESIAN_POINT ( 'NONE',  ( 5.299999999999999822, 5.388445916248354013E-16, 4.400000000000000355 ) ) ;
#472=AXIS2_PLACEMENT_3D ( 'NONE', #710, #4366, #2536 ) ;
#481=EDGE_CURVE ( 'NONE', #18883, #10793, #10717, .T. ) ;
#495=DIRECTION ( 'NONE',  ( 0.000000000000000000, 0.000000000000000000, 1.000000000000000000 ) ) ;
#579=CONICAL_SURFACE ( 'NONE', #20253, 3.309499999999999886, 0.7853981633974432830 ) ;
#581=B_SPLINE_CURVE_WITH_KNOTS ( 'NONE', 3,
 ( #18974, #14022, #18860, #15748, #7605, #8810 ),
 .UNSPECIFIED., .F., .F.,
 ( 4, 2, 4 ),
 ( 2.380733003139562229E-07, 0.001898835937927375716, 0.003797433802554437202 ),
 .UNSPECIFIED. ) ;
#648=EDGE_CURVE ( 'NONE', #8661, #6220, #4165, .T. ) ;
#673=DIRECTION ( 'NONE',  ( 1.000000000000000000, 0.000000000000000000, -0.000000000000000000 ) ) ;
#694=CARTESIAN_POINT ( 'NONE',  ( 0.5805565836007611225, 3.752776749732563477, 6.500000000000000000 ) ) ;
#696=DIRECTION ( 'NONE',  ( 1.000000000000000000, 0.000000000000000000, 0.000000000000000000 ) ) ;
#710=CARTESIAN_POINT ( 'NONE',  ( 4.700000000000000178, 6.500000000000000888, 0.000000000000000000 ) ) ;
#742=VECTOR ( 'NONE', #9615, 1000.000000000000114 ) ;
#771=AXIS2_PLACEMENT_3D ( 'NONE', #5394, #18697, #1965 ) ;
#774=EDGE_CURVE ( 'NONE', #19077, #15843, #2641, .T. ) ;
#794=ORIENTED_EDGE ( 'NONE', *, *, #7092, .F. ) ;
#808=CARTESIAN_POINT ( 'NONE',  ( 0.000000000000000000, 0.000000000000000000, 0.000000000000000000 ) ) ;
#830=VECTOR ( 'NONE', #8957, 1000.000000000000000 ) ;
#855=ADVANCED_FACE ( 'NONE', ( #12574 ), #17645, .F. ) ;
#878=EDGE_CURVE ( 'NONE', #5613, #19077, #11132, .T. ) ;
#887=APPLICATION_CONTEXT ( 'automotive_design' ) ;
#910=EDGE_CURVE ( 'NONE', #13843, #4925, #3656, .T. ) ;
#924=CIRCLE ( 'NONE', #10232, 6.500000000000000888 ) ;
#959=DIRECTION ( 'NONE',  ( 0.000000000000000000, 0.000000000000000000, -1.000000000000000000 ) ) ;
#963=AXIS2_PLACEMENT_3D ( 'NONE', #5944, #6051, #12561 ) ;
#1006=ORIENTED_EDGE ( 'NONE', *, *, #6483, .F. ) ;
#1011=CARTESIAN_POINT ( 'NONE',  ( -1.084202172485504434E-15, -5.948846446048903225, 2.696295709017763720 ) ) ;
#1024=DIRECTION ( 'NONE',  ( 1.000000000000000000, 0.000000000000000000, -0.000000000000000000 ) ) ;
#1035=CARTESIAN_POINT ( 'NONE',  ( 0.000000000000000000, 0.000000000000000000, 0.000000000000000000 ) ) ;
#1074=CARTESIAN_POINT ( 'NONE',  ( 5.700000000000000178, 0.000000000000000000, -4.400000000000000355 ) ) ;
#1088=CARTESIAN_POINT ( 'NONE',  ( 20.60949999999999349, 0.000000000000000000, 0.000000000000000000 ) ) ;
#1093=ORIENTED_EDGE ( 'NONE', *, *, #16695, .T. ) ;
#1109=ORIENTED_EDGE ( 'NONE', *, *, #1652, .F. ) ;
#1178=ADVANCED_FACE ( 'NONE', ( #9151 ), #8299, .T. ) ;
#1193=ORIENTED_EDGE ( 'NONE', *, *, #173, .T. ) ;
#1237=ORIENTED_EDGE ( 'NONE', *, *, #20816, .F. ) ;
#1260=ORIENTED_EDGE ( 'NONE', *, *, #878, .F. ) ;
#1278=LINE ( 'NONE', #8067, #9545 ) ;
#1301=EDGE_CURVE ( 'NONE', #2614, #5342, #7256, .T. ) ;
#1304=AXIS2_PLACEMENT_3D ( 'NONE', #13978, #5727, #14081 ) ;
#1311=EDGE_LOOP ( 'NONE', ( #5524, #18269, #18060, #3020, #1237, #19215 ) ) ;
#1331=DIRECTION ( 'NONE',  ( 0.000000000000000000, 0.000000000000000000, -1.000000000000000000 ) ) ;
#1373=ORIENTED_EDGE ( 'NONE', *, *, #878, .T. ) ;
#1458=DIRECTION ( 'NONE',  ( 1.000000000000000000, 0.000000000000000000, 0.000000000000000000 ) ) ;
#1464=LINE ( 'NONE', #6207, #13909 ) ;
#1492=DIRECTION ( 'NONE',  ( -1.000000000000000000, -0.000000000000000000, -0.000000000000000000 ) ) ;
#1516=DIRECTION ( 'NONE',  ( 1.000000000000000000, 0.000000000000000000, -0.000000000000000000 ) ) ;
#1550=EDGE_LOOP ( 'NONE', ( #21256, #5936, #20102 ) ) ;
#1576=CYLINDRICAL_SURFACE ( 'NONE', #4381, 6.500000000000000888 ) ;
#1625=DIRECTION ( 'NONE',  ( -0.000000000000000000, 0.000000000000000000, -1.000000000000000000 ) ) ;
#1646=VECTOR ( 'NONE', #9638, 1000.000000000000114 ) ;
#1652=EDGE_CURVE ( 'NONE', #9090, #12399, #581, .T. ) ;
#1656=CARTESIAN_POINT ( 'NONE',  ( 21.30000000000000071, 0.000000000000000000, 0.000000000000000000 ) ) ;
#1676=PLANE ( 'NONE',  #10600 ) ;
#1682=CARTESIAN_POINT ( 'NONE',  ( 20.60949999999999349, 4.898587196589412829E-16, -4.000000000000000000 ) ) ;
#1705=DIRECTION ( 'NONE',  ( -1.000000000000000000, -0.000000000000000000, -0.000000000000000000 ) ) ;
#1742=ORIENTED_EDGE ( 'NONE', *, *, #6387, .F. ) ;
#1743=DIRECTION ( 'NONE',  ( -1.000000000000000000, -0.000000000000000000, -0.000000000000000000 ) ) ;
#1788=CARTESIAN_POINT ( 'NONE',  ( 4.700000000000000178, 0.000000000000000000, 6.500000000000000888 ) ) ;
#1793=FACE_OUTER_BOUND ( 'NONE', #19145, .T. ) ;
#1850=DIRECTION ( 'NONE',  ( 0.000000000000000000, 0.000000000000000000, -1.000000000000000000 ) ) ;
#1857=CARTESIAN_POINT ( 'NONE',  ( 4.700000000000000178, 0.000000000000000000, 0.000000000000000000 ) ) ;
#1866=AXIS2_PLACEMENT_3D ( 'NONE', #11748, #1705, #13278 ) ;
#1938=ORIENTED_EDGE ( 'NONE', *, *, #19532, .F. ) ;
#1945=EDGE_LOOP ( 'NONE', ( #2595, #4010, #7835, #17534 ) ) ;
#1965=DIRECTION ( 'NONE',  ( 0.000000000000000000, 0.000000000000000000, -1.000000000000000000 ) ) ;
#1996=CARTESIAN_POINT ( 'NONE',  ( 4.700000000000000178, 0.000000000000000000, 0.000000000000000000 ) ) ;
#2067=EDGE_LOOP ( 'NONE', ( #9854, #18586 ) ) ;
#2116=VERTEX_POINT ( 'NONE', #1788 ) ;
#2146=ORIENTED_EDGE ( 'NONE', *, *, #8477, .F. ) ;
#2240=CARTESIAN_POINT ( 'NONE',  ( 0.4037800551813722216, -4.058962678540097180, 5.969670414742689779 ) ) ;
#2248=ORIENTED_EDGE ( 'NONE', *, *, #13331, .F. ) ;
#2267=CARTESIAN_POINT ( 'NONE',  ( 0.5805565836007647862, 7.505553499465139389, 2.227827669841787811E-16 ) ) ;
#2311=DIRECTION ( 'NONE',  ( -1.000000000000000000, -0.000000000000000000, -0.000000000000000000 ) ) ;
#2403=VERTEX_POINT ( 'NONE', #16555 ) ;
#2419=DIRECTION ( 'NONE',  ( 0.000000000000000000, 0.000000000000000000, 1.000000000000000000 ) ) ;
#2434=CARTESIAN_POINT ( 'NONE',  ( 5.299999999999999822, 3.752776749732560368, -6.499999999999999112 ) ) ;
#2442=DIRECTION ( 'NONE',  ( 1.000000000000000000, 0.000000000000000000, 0.000000000000000000 ) ) ;
#2504=CIRCLE ( 'NONE', #4571, 4.000000000000000000 ) ;
#2508=ORIENTED_EDGE ( 'NONE', *, *, #5828, .T. ) ;
#2510=DIRECTION ( 'NONE',  ( 1.000000000000000000, 0.000000000000000000, -0.000000000000000000 ) ) ;
#2536=DIRECTION ( 'NONE',  ( 0.000000000000000000, 0.000000000000000000, -1.000000000000000000 ) ) ;
#2538=CARTESIAN_POINT ( 'NONE',  ( 4.700000000000000178, 3.752776749732563033, 6.500000000000000000 ) ) ;
#2544=VECTOR ( 'NONE', #16108, 1000.000000000000114 ) ;
#2572=DIRECTION ( 'NONE',  ( 1.000000000000000000, 0.000000000000000000, 0.000000000000000000 ) ) ;
#2595=ORIENTED_EDGE ( 'NONE', *, *, #6720, .T. ) ;
#2614=VERTEX_POINT ( 'NONE', #2267 ) ;
#2615=DIRECTION ( 'NONE',  ( 1.000000000000000000, 0.000000000000000000, -0.000000000000000000 ) ) ;
#2641=B_SPLINE_CURVE_WITH_KNOTS ( 'NONE', 3,
 ( #21002, #9201, #19269, #19168, #1011, #106 ),
 .UNSPECIFIED., .F., .F.,
 ( 4, 2, 4 ),
 ( 2.380733003134506766E-07, 0.001898835937927388726, 0.003797433802554464090 ),
 .UNSPECIFIED. ) ;
#2682=CARTESIAN_POINT ( 'NONE',  ( 0.5805565836007715586, -7.505553499465150935, -4.964436717930768604E-16 ) ) ;
#2690=DIRECTION ( 'NONE',  ( 1.000000000000000000, 0.000000000000000000, -0.000000000000000000 ) ) ;
#2730=DIRECTION ( 'NONE',  ( 0.000000000000000000, -0.5000000000000007772, 0.8660254037844381525 ) ) ;
#2750=EDGE_LOOP ( 'NONE', ( #15105, #18089, #11435, #2248 ) ) ;
#2766=DIRECTION ( 'NONE',  ( 0.000000000000000000, 0.000000000000000000, -1.000000000000000000 ) ) ;
#2832=FACE_OUTER_BOUND ( 'NONE', #2750, .T. ) ;
#2836=EDGE_CURVE ( 'NONE', #5613, #21078, #16037, .T. ) ;
#2847=EDGE_CURVE ( 'NONE', #21308, #18480, #18777, .T. ) ;
#2939=DIRECTION ( 'NONE',  ( -0.7071067811865511255, 8.659560562354889717E-17, -0.7071067811865440200 ) ) ;
#2996=CARTESIAN_POINT ( 'NONE',  ( -5.085585815314819236E-15, 5.948846446048898784, -2.696295709017757503 ) ) ;
#3020=ORIENTED_EDGE ( 'NONE', *, *, #8089, .F. ) ;
#3061=VERTEX_POINT ( 'NONE', #9902 ) ;
#3134=AXIS2_PLACEMENT_3D ( 'NONE', #7876, #7454, #20884 ) ;
#3167=DIRECTION ( 'NONE',  ( 0.000000000000000000, -0.5000000000000018874, -0.8660254037844374864 ) ) ;
#3175=DIRECTION ( 'NONE',  ( 1.000000000000000000, 0.000000000000000000, -0.000000000000000000 ) ) ;
#3277=ADVANCED_FACE ( 'NONE', ( #4782 ), #8237, .T. ) ;
#3281=EDGE_CURVE ( 'NONE', #11550, #19077, #6400, .T. ) ;
#3444=EDGE_LOOP ( 'NONE', ( #12402, #11887, #11784, #15491 ) ) ;
#3479=CARTESIAN_POINT ( 'NONE',  ( 4.700000000000000178, 0.000000000000000000, 0.000000000000000000 ) ) ;
#3525=ORIENTED_EDGE ( 'NONE', *, *, #18276, .T. ) ;
#3546=ADVANCED_FACE ( 'NONE', ( #12133 ), #18103, .T. ) ;
#3630=ORIENTED_EDGE ( 'NONE', *, *, #19803, .T. ) ;
#3635=CARTESIAN_POINT ( 'NONE',  ( 4.700000000000000178, 3.752776749732560368, -6.499999999999999112 ) ) ;
#3656=LINE ( 'NONE', #13404, #416 ) ;
#3693=ORIENTED_EDGE ( 'NONE', *, *, #17226, .F. ) ;
#3699=DIRECTION ( 'NONE',  ( 0.000000000000000000, 0.000000000000000000, -1.000000000000000000 ) ) ;
#3737=EDGE_CURVE ( 'NONE', #21308, #4925, #2504, .T. ) ;
#3749=ADVANCED_FACE ( 'NONE', ( #12570 ), #7358, .T. ) ;
#3756=AXIS2_PLACEMENT_3D ( 'NONE', #6868, #20504, #8492 ) ;
#3772=LINE ( 'NONE', #5608, #830 ) ;
#3788=ADVANCED_FACE ( 'NONE', ( #2832 ), #14605, .F. ) ;
#3818=LINE ( 'NONE', #7379, #18686 ) ;
#3819=CARTESIAN_POINT ( 'NONE',  ( 0.5805565836007597902, 3.752776749732560368, -6.499999999999999112 ) ) ;
#3858=ORIENTED_EDGE ( 'NONE', *, *, #14840, .F. ) ;
#3869=( NAMED_UNIT ( * ) SI_UNIT ( $, .STERADIAN. ) SOLID_ANGLE_UNIT ( ) );
#3891=DIRECTION ( 'NONE',  ( 0.000000000000000000, 0.000000000000000000, -1.000000000000000000 ) ) ;
#3919=FACE_OUTER_BOUND ( 'NONE', #20148, .T. ) ;
#3954=CARTESIAN_POINT ( 'NONE',  ( 0.000000000000000000, 5.629165124598848102, 3.250000000000005329 ) ) ;
#3963=VERTEX_POINT ( 'NONE', #16562 ) ;
#4010=ORIENTED_EDGE ( 'NONE', *, *, #6564, .T. ) ;
#4061=EDGE_CURVE ( 'NONE', #12399, #2614, #14247, .T. ) ;
#4070=ORIENTED_EDGE ( 'NONE', *, *, #13331, .T. ) ;
#4076=SHAPE_REPRESENTATION ( 'hex screw gradeab_iso_ISO 4017 - M8 x 16-N', ( #12794 ), #12451 ) ;
#4116=LINE ( 'NONE', #7460, #8398 ) ;
#4159=CARTESIAN_POINT ( 'NONE',  ( 0.1061556211655317883, 4.836380039389415408, -4.623144047065555817 ) ) ;
#4164=CARTESIAN_POINT ( 'NONE',  ( 0.5805565836007611225, -3.752776749732563033, 6.500000000000000000 ) ) ;
#4165=CIRCLE ( 'NONE', #6920, 3.309499999999999886 ) ;
#4253=CARTESIAN_POINT ( 'NONE',  ( 0.000000000000000000, 0.000000000000000000, 0.000000000000000000 ) ) ;
#4261=ORIENTED_EDGE ( 'NONE', *, *, #20722, .F. ) ;
#4279=CARTESIAN_POINT ( 'NONE',  ( 0.000000000000000000, -5.629165124598843661, 3.250000000000012434 ) ) ;
#4346=CARTESIAN_POINT ( 'NONE',  ( 5.299999999999999822, -3.752776749732576356, -6.499999999999999112 ) ) ;
#4366=DIRECTION ( 'NONE',  ( 1.000000000000000000, 0.000000000000000000, 0.000000000000000000 ) ) ;
#4381=AXIS2_PLACEMENT_3D ( 'NONE', #18322, #15099, #5236 ) ;
#4395=ORIENTED_EDGE ( 'NONE', *, *, #6483, .T. ) ;
#4399=PLANE ( 'NONE',  #16960 ) ;
#4440=ORIENTED_EDGE ( 'NONE', *, *, #17782, .F. ) ;
#4453=EDGE_CURVE ( 'NONE', #21078, #13633, #5181, .T. ) ;
#4525=AXIS2_PLACEMENT_3D ( 'NONE', #4747, #17940, #1850 ) ;
#4571=AXIS2_PLACEMENT_3D ( 'NONE', #9094, #2510, #7683 ) ;
#4590=CARTESIAN_POINT ( 'NONE',  ( 0.2578475836320679448, 4.367703157927326885, -5.434916218090832807 ) ) ;
#4616=CARTESIAN_POINT ( 'NONE',  ( 0.4042117618287677239, -3.141900367811078620, 6.500000000000001776 ) ) ;
#4655=ORIENTED_EDGE ( 'NONE', *, *, #7092, .T. ) ;
#4656=ORIENTED_EDGE ( 'NONE', *, *, #17736, .F. ) ;
#4665=EDGE_CURVE ( 'NONE', #11550, #11897, #1464, .T. ) ;
#4728=AXIS2_PLACEMENT_3D ( 'NONE', #14008, #5443, #15518 ) ;
#4747=CARTESIAN_POINT ( 'NONE',  ( 5.299999999999999822, 0.000000000000000000, 0.000000000000000000 ) ) ;
#4782=FACE_OUTER_BOUND ( 'NONE', #9469, .T. ) ;
#4798=DIRECTION ( 'NONE',  ( 0.000000000000000000, 0.000000000000000000, 1.000000000000000000 ) ) ;
#4817=CARTESIAN_POINT ( 'NONE',  ( 0.2573354458087834251, 6.889406814520511624, -1.067197363239225316 ) ) ;
#4823=DIRECTION ( 'NONE',  ( 1.000000000000000000, 0.000000000000000000, -0.000000000000000000 ) ) ;
#4889=ORIENTED_EDGE ( 'NONE', *, *, #14840, .T. ) ;
#4917=ADVANCED_FACE ( 'NONE', ( #18527 ), #12480, .T. ) ;
#4925=VERTEX_POINT ( 'NONE', #10622 ) ;
#4938=EDGE_CURVE ( 'NONE', #15214, #6373, #3818, .T. ) ;
#4956=DIRECTION ( 'NONE',  ( 0.000000000000000000, 0.000000000000000000, 1.000000000000000000 ) ) ;
#4958=EDGE_CURVE ( 'NONE', #8381, #2116, #17997, .T. ) ;
#4971=ORIENTED_EDGE ( 'NONE', *, *, #14181, .T. ) ;
#5027=EDGE_LOOP ( 'NONE', ( #5294, #6587, #12650, #8017, #11006, #18386 ) ) ;
#5059=DIRECTION ( 'NONE',  ( -1.000000000000000000, -0.000000000000000000, -0.000000000000000000 ) ) ;
#5069=VECTOR ( 'NONE', #15022, 1000.000000000000000 ) ;
#5071=DIRECTION ( 'NONE',  ( 0.000000000000000000, 0.000000000000000000, -1.000000000000000000 ) ) ;
#5106=ORIENTED_EDGE ( 'NONE', *, *, #13678, .T. ) ;
#5132=FACE_OUTER_BOUND ( 'NONE', #10074, .T. ) ;
#5151=FACE_OUTER_BOUND ( 'NONE', #3444, .T. ) ;
#5171=CARTESIAN_POINT ( 'NONE',  ( 0.4037800551813805483, -7.199367570657614124, -0.5303295852573159941 ) ) ;
#5180=DIRECTION ( 'NONE',  ( -1.000000000000000000, 0.000000000000000000, -0.000000000000000000 ) ) ;
#5181=B_SPLINE_CURVE_WITH_KNOTS ( 'NONE', 3,
 ( #20087, #18555, #9904, #16525, #5257, #8277 ),
 .UNSPECIFIED., .F., .F.,
 ( 4, 2, 4 ),
 ( 0.02294124189192014301, 0.02484059228024679267, 0.02673994266857344232 ),
 .UNSPECIFIED. ) ;
#5205=DIRECTION ( 'NONE',  ( 0.000000000000000000, -0.5000000000000018874, -0.8660254037844374864 ) ) ;
#5213=AXIS2_PLACEMENT_3D ( 'NONE', #21198, #5180, #11776 ) ;
#5236=DIRECTION ( 'NONE',  ( 0.000000000000000000, 0.000000000000000000, 1.000000000000000000 ) ) ;
#5257=CARTESIAN_POINT ( 'NONE',  ( 0.4042117618287694447, -3.141900367811087502, -6.500000000000000000 ) ) ;
#5294=ORIENTED_EDGE ( 'NONE', *, *, #13678, .F. ) ;
#5342=VERTEX_POINT ( 'NONE', #5973 ) ;
#5372=CARTESIAN_POINT ( 'NONE',  ( 0.000000000000000000, -5.629165124598848990, -3.250000000000004441 ) ) ;
#5380=EDGE_CURVE ( 'NONE', #21185, #9090, #13228, .T. ) ;
#5394=CARTESIAN_POINT ( 'NONE',  ( 0.000000000000000000, 0.000000000000000000, 0.000000000000000000 ) ) ;
#5443=DIRECTION ( 'NONE',  ( -0.000000000000000000, 1.000000000000000000, -1.224646799147353207E-16 ) ) ;
#5466=CARTESIAN_POINT ( 'NONE',  ( 0.2578475836320708869, -4.367703157927327773, 5.434916218090835471 ) ) ;
#5470=ADVANCED_FACE ( 'NONE', ( #8654 ), #10486, .F. ) ;
#5499=ORIENTED_EDGE ( 'NONE', *, *, #21202, .T. ) ;
#5524=ORIENTED_EDGE ( 'NONE', *, *, #173, .F. ) ;
#5592=EDGE_CURVE ( 'NONE', #11897, #18587, #12874, .T. ) ;
#5602=ADVANCED_FACE ( 'NONE', ( #6052 ), #9188, .F. ) ;
#5608=CARTESIAN_POINT ( 'NONE',  ( 0.000000000000000000, 4.898587196589412829E-16, -4.000000000000000000 ) ) ;
#5613=VERTEX_POINT ( 'NONE', #6262 ) ;
#5614=ADVANCED_FACE ( 'NONE', ( #20665 ), #12767, .F. ) ;
#5661=ORIENTED_EDGE ( 'NONE', *, *, #13857, .F. ) ;
#5667=CARTESIAN_POINT ( 'NONE',  ( 4.700000000000000178, -5.629165124598848990, -3.250000000000005329 ) ) ;
#5727=DIRECTION ( 'NONE',  ( -1.000000000000000000, -0.000000000000000000, -0.000000000000000000 ) ) ;
#5741=VECTOR ( 'NONE', #5205, 1000.000000000000227 ) ;
#5780=CARTESIAN_POINT ( 'NONE',  ( 0.4033376246892514949, -4.059728990630810941, -5.968343123267132455 ) ) ;
#5804=CARTESIAN_POINT ( 'NONE',  ( 0.2565376335220200255, -2.516992571281980950, 6.500000000000002665 ) ) ;
#5828=EDGE_CURVE ( 'NONE', #21078, #5342, #21104, .T. ) ;
#5838=ADVANCED_BREP_SHAPE_REPRESENTATION ( '', ( #11980, #12794 ), #12451 ) ;
#5844=EDGE_CURVE ( 'NONE', #18480, #10315, #13859, .T. ) ;
#5860=ADVANCED_FACE ( 'NONE', ( #8310 ), #20755, .F. ) ;
#5872=EDGE_CURVE ( 'NONE', #18587, #10793, #20002, .T. ) ;
#5877=DIRECTION ( 'NONE',  ( -1.000000000000000000, -0.000000000000000000, -0.000000000000000000 ) ) ;
#5903=PRODUCT_DEFINITION_FORMATION_WITH_SPECIFIED_SOURCE ( 'ANY', '', #7491, .NOT_KNOWN. ) ;
#5916=DIRECTION ( 'NONE',  ( 1.000000000000000000, 0.000000000000000000, -0.000000000000000000 ) ) ;
#5918=ADVANCED_FACE ( 'NONE', ( #5, #21297 ), #6469, .T. ) ;
#5936=ORIENTED_EDGE ( 'NONE', *, *, #1301, .T. ) ;
#5944=CARTESIAN_POINT ( 'NONE',  ( 21.30000000000000071, 0.000000000000000000, 0.000000000000000000 ) ) ;
#5973=CARTESIAN_POINT ( 'NONE',  ( 0.000000000000000000, 5.629165124598846326, -3.250000000000007550 ) ) ;
#5998=CARTESIAN_POINT ( 'NONE',  ( 5.299999999999999822, 0.000000000000000000, 0.000000000000000000 ) ) ;
#5999=DIRECTION ( 'NONE',  ( 0.000000000000000000, -1.000000000000000000, 0.000000000000000000 ) ) ;
#6001=ADVANCED_FACE ( 'NONE', ( #16232 ), #13413, .F. ) ;
#6037=ORIENTED_EDGE ( 'NONE', *, *, #2836, .F. ) ;
#6051=DIRECTION ( 'NONE',  ( -1.000000000000000000, -0.000000000000000000, -0.000000000000000000 ) ) ;
#6052=FACE_OUTER_BOUND ( 'NONE', #5027, .T. ) ;
#6096=CARTESIAN_POINT ( 'NONE',  ( 0.05533025579362596535, -4.993776679985865385, -4.350525068611872825 ) ) ;
#6116=EDGE_CURVE ( 'NONE', #5342, #12399, #20061, .T. ) ;
#6207=CARTESIAN_POINT ( 'NONE',  ( 4.700000000000000178, -3.752776749732576356, -6.499999999999999112 ) ) ;
#6220=VERTEX_POINT ( 'NONE', #20037 ) ;
#6235=AXIS2_PLACEMENT_3D ( 'NONE', #19220, #2572, #14152 ) ;
#6260=EDGE_CURVE ( 'NONE', #3963, #9090, #4116, .T. ) ;
#6262=CARTESIAN_POINT ( 'NONE',  ( 0.000000000000000000, -5.629165124598848990, -3.250000000000004441 ) ) ;
#6266=ORIENTED_EDGE ( 'NONE', *, *, #6387, .T. ) ;
#6373=VERTEX_POINT ( 'NONE', #20671 ) ;
#6387=EDGE_CURVE ( 'NONE', #12984, #21078, #19920, .T. ) ;
#6397=ORIENTED_EDGE ( 'NONE', *, *, #21057, .T. ) ;
#6400=LINE ( 'NONE', #11379, #19840 ) ;
#6421=ORIENTED_EDGE ( 'NONE', *, *, #4665, .T. ) ;
#6435=CIRCLE ( 'NONE', #4728, 0.4000000000000001887 ) ;
#6450=VECTOR ( 'NONE', #8707, 1000.000000000000000 ) ;
#6469=PLANE ( 'NONE',  #15234 ) ;
#6483=EDGE_CURVE ( 'NONE', #11897, #8381, #130, .T. ) ;
#6564=EDGE_CURVE ( 'NONE', #12838, #21308, #3772, .T. ) ;
#6587=ORIENTED_EDGE ( 'NONE', *, *, #20816, .T. ) ;
#6633=DIRECTION ( 'NONE',  ( 1.000000000000000000, 0.000000000000000000, 0.000000000000000000 ) ) ;
#6638=VECTOR ( 'NONE', #17466, 1000.000000000000000 ) ;
#6669=AXIS2_PLACEMENT_3D ( 'NONE', #1857, #1743, #18483 ) ;
#6684=PLANE ( 'NONE',  #21300 ) ;
#6687=AXIS2_PLACEMENT_3D ( 'NONE', #10778, #5916, #12527 ) ;
#6703=EDGE_CURVE ( 'NONE', #18883, #15214, #9281, .T. ) ;
#6720=EDGE_CURVE ( 'NONE', #13843, #12838, #13253, .T. ) ;
#6802=CARTESIAN_POINT ( 'NONE',  ( 0.4053525175235877520, 3.145852061455921778, -6.500000000000000000 ) ) ;
#6846=DIRECTION ( 'NONE',  ( 0.000000000000000000, 0.000000000000000000, -1.000000000000000000 ) ) ;
#6868=CARTESIAN_POINT ( 'NONE',  ( 0.000000000000000000, 0.000000000000000000, 0.000000000000000000 ) ) ;
#6920=AXIS2_PLACEMENT_3D ( 'NONE', #13297, #7788, #4956 ) ;
#6940=DIRECTION ( 'NONE',  ( -1.000000000000000000, -0.000000000000000000, -0.000000000000000000 ) ) ;
#7019=ORIENTED_EDGE ( 'NONE', *, *, #8089, .T. ) ;
#7038=ADVANCED_FACE ( 'NONE', ( #211 ), #8805, .T. ) ;
#7092=EDGE_CURVE ( 'NONE', #2403, #12984, #7389, .T. ) ;
#7101=CARTESIAN_POINT ( 'NONE',  ( 2.234578793975251082E-15, -5.788408252967910173, -2.974182810908600594 ) ) ;
#7111=CIRCLE ( 'NONE', #19221, 6.500000000000000888 ) ;
#7131=CIRCLE ( 'NONE', #19237, 4.000000000000000000 ) ;
#7256=B_SPLINE_CURVE_WITH_KNOTS ( 'NONE', 3,
 ( #9788, #19747, #4817, #14372, #2996, #18121 ),
 .UNSPECIFIED., .F., .F.,
 ( 4, 2, 4 ),
 ( 2.380733003136581732E-07, 0.001898835937927382872, 0.003797433802554452380 ),
 .UNSPECIFIED. ) ;
#7264=CARTESIAN_POINT ( 'NONE',  ( 0.000000000000000000, 0.000000000000000000, 0.000000000000000000 ) ) ;
#7272=VECTOR ( 'NONE', #19893, 1000.000000000000000 ) ;
#7280=AXIS2_PLACEMENT_3D ( 'NONE', #4346, #17539, #2730 ) ;
#7330=ORIENTED_EDGE ( 'NONE', *, *, #4958, .F. ) ;
#7331=EDGE_LOOP ( 'NONE', ( #6397, #5106, #9467 ) ) ;
#7358=PLANE ( 'NONE',  #11481 ) ;
#7379=CARTESIAN_POINT ( 'NONE',  ( 4.700000000000000178, 7.505553499465139389, 0.000000000000000000 ) ) ;
#7389=LINE ( 'NONE', #2434, #147 ) ;
#7453=FACE_OUTER_BOUND ( 'NONE', #13376, .T. ) ;
#7454=DIRECTION ( 'NONE',  ( 0.000000000000000000, 0.8660254037844375974, -0.5000000000000018874 ) ) ;
#7460=CARTESIAN_POINT ( 'NONE',  ( 5.299999999999999822, 3.752776749732563033, 6.500000000000000000 ) ) ;
#7491=PRODUCT ( 'hex screw gradeab_iso_ISO 4017 - M8 x 16-N', 'hex screw gradeab_iso_ISO 4017 - M8 x 16-N', '', ( #15190 ) ) ;
#7534=CARTESIAN_POINT ( 'NONE',  ( 0.5805565836007647862, 7.505553499465139389, 2.227827669841787811E-16 ) ) ;
#7566=EDGE_LOOP ( 'NONE', ( #1093, #15920, #4889 ) ) ;
#7570=EDGE_LOOP ( 'NONE', ( #14966, #6266, #2508 ) ) ;
#7605=CARTESIAN_POINT ( 'NONE',  ( -4.001383642829314802E-15, 5.309483803148796532, 3.803704290982252267 ) ) ;
#7610=CARTESIAN_POINT ( 'NONE',  ( 0.000000000000000000, 5.629165124598846326, -3.250000000000007550 ) ) ;
#7613=DIRECTION ( 'NONE',  ( 0.000000000000000000, -0.5000000000000011102, -0.8660254037844379305 ) ) ;
#7625=ORIENTED_EDGE ( 'NONE', *, *, #9827, .F. ) ;
#7683=DIRECTION ( 'NONE',  ( 0.000000000000000000, 0.000000000000000000, -1.000000000000000000 ) ) ;
#7745=CARTESIAN_POINT ( 'NONE',  ( 0.000000000000000000, 0.000000000000000000, 6.500000000000000000 ) ) ;
#7763=ORIENTED_EDGE ( 'NONE', *, *, #14612, .T. ) ;
#7784=DIRECTION ( 'NONE',  ( 0.000000000000000000, 0.000000000000000000, -1.000000000000000000 ) ) ;
#7788=DIRECTION ( 'NONE',  ( -1.000000000000000000, -0.000000000000000000, -0.000000000000000000 ) ) ;
#7809=ORIENTED_EDGE ( 'NONE', *, *, #17226, .T. ) ;
#7823=CARTESIAN_POINT ( 'NONE',  ( 0.01372220897661586593, 5.309964801958114045, -3.802871176606130277 ) ) ;
#7835=ORIENTED_EDGE ( 'NONE', *, *, #3737, .T. ) ;
#7876=CARTESIAN_POINT ( 'NONE',  ( 5.299999999999999822, -7.505553499465150047, 0.000000000000000000 ) ) ;
#7887=ORIENTED_EDGE ( 'NONE', *, *, #13857, .T. ) ;
#7924=CARTESIAN_POINT ( 'NONE',  ( 4.700000000000000178, 7.505553499465139389, 0.000000000000000000 ) ) ;
#7947=MECHANICAL_DESIGN_GEOMETRIC_PRESENTATION_REPRESENTATION('',(#12459),#390);
#8017=ORIENTED_EDGE ( 'NONE', *, *, #774, .F. ) ;
#8020=ORIENTED_EDGE ( 'NONE', *, *, #10448, .F. ) ;
#8059=CARTESIAN_POINT ( 'NONE',  ( 4.700000000000000178, 0.000000000000000000, 0.000000000000000000 ) ) ;
#8067=CARTESIAN_POINT ( 'NONE',  ( 5.299999999999999822, -3.752776749732576356, -6.499999999999999112 ) ) ;
#8088=CARTESIAN_POINT ( 'NONE',  ( 5.700000000000000178, 0.000000000000000000, 0.000000000000000000 ) ) ;
#8089=EDGE_CURVE ( 'NONE', #19525, #21185, #16334, .T. ) ;
#8136=CARTESIAN_POINT ( 'NONE',  ( 4.700000000000000178, 0.000000000000000000, 0.000000000000000000 ) ) ;
#8137=CARTESIAN_POINT ( 'NONE',  ( 4.700000000000000178, 3.752776749732563033, 6.500000000000000000 ) ) ;
#8164=CYLINDRICAL_SURFACE ( 'NONE', #1866, 4.000000000000000000 ) ;
#8170=B_SPLINE_CURVE_WITH_KNOTS ( 'NONE', 3,
 ( #7610, #21033, #7823, #9242, #4159, #4590, #14026, #17261 ),
 .UNSPECIFIED., .F., .F.,
 ( 4, 2, 2, 4 ),
 ( 0.003797433802554452380, 0.004743183970586248299, 0.005688934138618042050, 0.007580434474681631285 ),
 .UNSPECIFIED. ) ;
#8199=PRODUCT_DEFINITION_SHAPE ( 'NONE', 'NONE',  #8621 ) ;
#8225=CARTESIAN_POINT ( 'NONE',  ( 0.2595206531159287011, 2.531175536751829824, 6.499999999999999112 ) ) ;
#8237=PLANE ( 'NONE',  #10494 ) ;
#8254=CIRCLE ( 'NONE', #16570, 4.000000000000000000 ) ;
#8258=VERTEX_POINT ( 'NONE', #87 ) ;
#8277=CARTESIAN_POINT ( 'NONE',  ( 0.5805565836007642311, -3.752776749732576356, -6.499999999999999112 ) ) ;
#8299=CONICAL_SURFACE ( 'NONE', #6235, 6.500000000000000000, 1.047197551196600296 ) ;
#8310=FACE_OUTER_BOUND ( 'NONE', #14677, .T. ) ;
#8346=EDGE_LOOP ( 'NONE', ( #3693, #12704 ) ) ;
#8363=EDGE_CURVE ( 'NONE', #6373, #18883, #13087, .T. ) ;
#8381=VERTEX_POINT ( 'NONE', #21164 ) ;
#8398=VECTOR ( 'NONE', #15820, 1000.000000000000000 ) ;
#8420=DIRECTION ( 'NONE',  ( 1.000000000000000000, 0.000000000000000000, -0.000000000000000000 ) ) ;
#8431=CARTESIAN_POINT ( 'NONE',  ( 4.700000000000000178, 0.000000000000000000, -6.500000000000000000 ) ) ;
#8432=ORIENTED_EDGE ( 'NONE', *, *, #4061, .F. ) ;
#8469=FACE_OUTER_BOUND ( 'NONE', #7570, .T. ) ;
#8477=EDGE_CURVE ( 'NONE', #21185, #12399, #8924, .T. ) ;
#8492=DIRECTION ( 'NONE',  ( 0.000000000000000000, 0.000000000000000000, 1.000000000000000000 ) ) ;
#8531=CARTESIAN_POINT ( 'NONE',  ( 0.2595206531159274244, 2.531175536751827160, -6.499999999999999112 ) ) ;
#8564=DIRECTION ( 'NONE',  ( 0.000000000000000000, 0.000000000000000000, 1.000000000000000000 ) ) ;
#8621=PRODUCT_DEFINITION ( 'UNKNOWN', '', #5903, #145 ) ;
#8635=CARTESIAN_POINT ( 'NONE',  ( 0.05613245601076728708, 1.278525034532176585, -6.499999999999999112 ) ) ;
#8654=FACE_OUTER_BOUND ( 'NONE', #10603, .T. ) ;
#8661=VERTEX_POINT ( 'NONE', #12605 ) ;
#8666=ORIENTED_EDGE ( 'NONE', *, *, #5828, .F. ) ;
#8678=DIRECTION ( 'NONE',  ( 0.000000000000000000, 0.000000000000000000, 1.000000000000000000 ) ) ;
#8687=ADVANCED_FACE ( 'NONE', ( #20927 ), #17245, .T. ) ;
#8702=ORIENTED_EDGE ( 'NONE', *, *, #14057, .F. ) ;
#8707=DIRECTION ( 'NONE',  ( 0.000000000000000000, 1.000000000000000000, -0.000000000000000000 ) ) ;
#8774=AXIS2_PLACEMENT_3D ( 'NONE', #18511, #11917, #3699 ) ;
#8805=PLANE ( 'NONE',  #472 ) ;
#8810=CARTESIAN_POINT ( 'NONE',  ( 0.000000000000000000, 5.629165124598848102, 3.250000000000005329 ) ) ;
#8905=ORIENTED_EDGE ( 'NONE', *, *, #6720, .F. ) ;
#8924=CIRCLE ( 'NONE', #3756, 6.500000000000000000 ) ;
#8957=DIRECTION ( 'NONE',  ( -1.000000000000000000, -0.000000000000000000, -0.000000000000000000 ) ) ;
#8983=AXIS2_PLACEMENT_3D ( 'NONE', #14984, #11723, #18315 ) ;
#9054=SHAPE_REPRESENTATION_RELATIONSHIP ( 'NONE' , 'NONE' ,  #4076, #5838 ) ;
#9074=ADVANCED_FACE ( 'NONE', ( #3919 ), #20051, .T. ) ;
#9087=ORIENTED_EDGE ( 'NONE', *, *, #13469, .T. ) ;
#9090=VERTEX_POINT ( 'NONE', #694 ) ;
#9094=CARTESIAN_POINT ( 'NONE',  ( 5.700000000000000178, 0.000000000000000000, 0.000000000000000000 ) ) ;
#9147=FACE_OUTER_BOUND ( 'NONE', #7566, .T. ) ;
#9151=FACE_OUTER_BOUND ( 'NONE', #14705, .T. ) ;
#9168=EDGE_LOOP ( 'NONE', ( #12945, #16014, #14414 ) ) ;
#9188=PLANE ( 'NONE',  #3134 ) ;
#9195=EDGE_LOOP ( 'NONE', ( #14036, #4070 ) ) ;
#9201=CARTESIAN_POINT ( 'NONE',  ( 0.4033376246892552697, -7.198601258566911021, 0.5316568767328686551 ) ) ;
#9242=CARTESIAN_POINT ( 'NONE',  ( 0.06682554136337785777, 4.993536075455418555, -4.350941807883112133 ) ) ;
#9275=LINE ( 'NONE', #15891, #5741 ) ;
#9281=LINE ( 'NONE', #12858, #2544 ) ;
#9282=ORIENTED_EDGE ( 'NONE', *, *, #17736, .T. ) ;
#9283=ORIENTED_EDGE ( 'NONE', *, *, #14181, .F. ) ;
#9354=AXIS2_PLACEMENT_3D ( 'NONE', #1996, #6940, #8564 ) ;
#9369=AXIS2_PLACEMENT_3D ( 'NONE', #15623, #15308, #495 ) ;
#9379=DIRECTION ( 'NONE',  ( 0.000000000000000000, 0.000000000000000000, -1.000000000000000000 ) ) ;
#9408=CIRCLE ( 'NONE', #15654, 6.500000000000000888 ) ;
#9432=CARTESIAN_POINT ( 'NONE',  ( 5.299999999999999822, 0.000000000000000000, 0.000000000000000000 ) ) ;
#9446=FACE_OUTER_BOUND ( 'NONE', #1945, .T. ) ;
#9458=CARTESIAN_POINT ( 'NONE',  ( 0.000000000000000000, 0.000000000000000000, -6.499999999999999112 ) ) ;
#9467=ORIENTED_EDGE ( 'NONE', *, *, #4958, .T. ) ;
#9469=EDGE_LOOP ( 'NONE', ( #16059, #14779, #9087 ) ) ;
#9480=CARTESIAN_POINT ( 'NONE',  ( 0.5805565836007611225, -3.752776749732563033, 6.500000000000000000 ) ) ;
#9545=VECTOR ( 'NONE', #1492, 1000.000000000000000 ) ;
#9581=CONICAL_SURFACE ( 'NONE', #1304, 3.309499999999999886, 0.7853981633974432830 ) ;
#9598=DIRECTION ( 'NONE',  ( 0.000000000000000000, 0.000000000000000000, 1.000000000000000000 ) ) ;
#9615=DIRECTION ( 'NONE',  ( 0.000000000000000000, 0.5000000000000007772, -0.8660254037844381525 ) ) ;
#9636=( NAMED_UNIT ( * ) PLANE_ANGLE_UNIT ( ) SI_UNIT ( $, .RADIAN. ) );
#9638=DIRECTION ( 'NONE',  ( -0.000000000000000000, 0.5000000000000011102, 0.8660254037844379305 ) ) ;
#9661=CARTESIAN_POINT ( 'NONE',  ( 0.000000000000000000, 0.000000000000000000, 6.500000000000000000 ) ) ;
#9719=CARTESIAN_POINT ( 'NONE',  ( 4.700000000000000178, 3.752776749732560368, -6.499999999999999112 ) ) ;
#9740=DIRECTION ( 'NONE',  ( 0.000000000000000000, 0.5000000000000008882, -0.8660254037844381525 ) ) ;
#9744=CARTESIAN_POINT ( 'NONE',  ( 0.4053525175235895284, 3.145852061455926663, 6.499999999999999112 ) ) ;
#9750=ORIENTED_EDGE ( 'NONE', *, *, #481, .F. ) ;
#9788=CARTESIAN_POINT ( 'NONE',  ( 0.5805565836007647862, 7.505553499465139389, 2.227827669841787811E-16 ) ) ;
#9827=EDGE_CURVE ( 'NONE', #4925, #21308, #8254, .T. ) ;
#9829=CARTESIAN_POINT ( 'NONE',  ( 0.000000000000000000, 0.000000000000000000, -6.499999999999999112 ) ) ;
#9830=ORIENTED_EDGE ( 'NONE', *, *, #16695, .F. ) ;
#9854=ORIENTED_EDGE ( 'NONE', *, *, #19661, .T. ) ;
#9898=DIRECTION ( 'NONE',  ( -1.000000000000000000, -0.000000000000000000, -0.000000000000000000 ) ) ;
#9902=CARTESIAN_POINT ( 'NONE',  ( 5.299999999999999822, 0.000000000000000000, 6.500000000000000888 ) ) ;
#9904=CARTESIAN_POINT ( 'NONE',  ( 0.05458999538792617262, -1.264741368075143146, -6.499999999999999112 ) ) ;
#9959=CARTESIAN_POINT ( 'NONE',  ( -7.623296525288703052E-18, 0.6351314446054981966, 6.500000000000001776 ) ) ;
#10017=LINE ( 'NONE', #13607, #5069 ) ;
#10028=EDGE_LOOP ( 'NONE', ( #16057, #14683, #1260, #19023, #4440, #16186 ) ) ;
#10074=EDGE_LOOP ( 'NONE', ( #10658, #18330, #19501, #7330, #1006, #11028 ) ) ;
#10161=FACE_OUTER_BOUND ( 'NONE', #19317, .T. ) ;
#10220=CARTESIAN_POINT ( 'NONE',  ( 0.000000000000000000, 0.000000000000000000, 6.500000000000000888 ) ) ;
#10232=AXIS2_PLACEMENT_3D ( 'NONE', #4253, #1024, #12792 ) ;
#10246=VECTOR ( 'NONE', #14358, 1000.000000000000000 ) ;
#10315=VERTEX_POINT ( 'NONE', #433 ) ;
#10441=LINE ( 'NONE', #20516, #16481 ) ;
#10448=EDGE_CURVE ( 'NONE', #8661, #12838, #16035, .T. ) ;
#10453=CARTESIAN_POINT ( 'NONE',  ( 0.1061556211655396709, -6.421950209808290566, -1.876855952934453731 ) ) ;
#10486=PLANE ( 'NONE',  #10732 ) ;
#10494=AXIS2_PLACEMENT_3D ( 'NONE', #158, #18192, #21235 ) ;
#10563=CARTESIAN_POINT ( 'NONE',  ( 0.2578475836320711090, 6.890627091270371984, 1.065083781909172744 ) ) ;
#10600=AXIS2_PLACEMENT_3D ( 'NONE', #14876, #1458, #16710 ) ;
#10603=EDGE_LOOP ( 'NONE', ( #8666, #6037, #20525, #4656, #10897, #19218 ) ) ;
#10622=CARTESIAN_POINT ( 'NONE',  ( 5.700000000000000178, 0.000000000000000000, 4.000000000000000000 ) ) ;
#10658=ORIENTED_EDGE ( 'NONE', *, *, #21202, .F. ) ;
#10670=CARTESIAN_POINT ( 'NONE',  ( 0.01372220897661636727, 5.948365447239582160, 2.697128823393878161 ) ) ;
#10717=CIRCLE ( 'NONE', #9354, 6.500000000000000888 ) ;
#10732=AXIS2_PLACEMENT_3D ( 'NONE', #15487, #673, #20237 ) ;
#10752=CARTESIAN_POINT ( 'NONE',  ( 0.5805565836007611225, -3.752776749732563033, 6.500000000000000000 ) ) ;
#10754=ADVANCED_FACE ( 'NONE', ( #10161 ), #19742, .T. ) ;
#10755=CARTESIAN_POINT ( 'NONE',  ( 4.700000000000000178, -3.752776749732563033, 6.500000000000000000 ) ) ;
#10778=CARTESIAN_POINT ( 'NONE',  ( 0.000000000000000000, 0.000000000000000000, 0.000000000000000000 ) ) ;
#10793=VERTEX_POINT ( 'NONE', #8431 ) ;
#10811=CARTESIAN_POINT ( 'NONE',  ( 4.700000000000000178, -3.752776749732576356, -6.499999999999999112 ) ) ;
#10822=CARTESIAN_POINT ( 'NONE',  ( 5.700000000000000178, 0.000000000000000000, 0.000000000000000000 ) ) ;
#10897=ORIENTED_EDGE ( 'NONE', *, *, #8477, .T. ) ;
#10964=CARTESIAN_POINT ( 'NONE',  ( 0.000000000000000000, 0.000000000000000000, 0.000000000000000000 ) ) ;
#10966=DIRECTION ( 'NONE',  ( 1.000000000000000000, 0.000000000000000000, -0.000000000000000000 ) ) ;
#10992=DIRECTION ( 'NONE',  ( 0.000000000000000000, -1.000000000000000000, 0.000000000000000000 ) ) ;
#11006=ORIENTED_EDGE ( 'NONE', *, *, #3281, .F. ) ;
#11028=ORIENTED_EDGE ( 'NONE', *, *, #13469, .F. ) ;
#11132=B_SPLINE_CURVE_WITH_KNOTS ( 'NONE', 3,
 ( #5372, #7101, #19882, #19991, #10453, #20103, #5171, #15033 ),
 .UNSPECIFIED., .F., .F.,
 ( 4, 2, 2, 4 ),
 ( 0.003797433802554430696, 0.004743183970586230085, 0.005688934138618029039, 0.007580434474681626081 ),
 .UNSPECIFIED. ) ;
#11164=AXIS2_PLACEMENT_3D ( 'NONE', #5998, #10966, #2766 ) ;
#11213=DIRECTION ( 'NONE',  ( 0.000000000000000000, 0.000000000000000000, -1.000000000000000000 ) ) ;
#11276=CYLINDRICAL_SURFACE ( 'NONE', #14904, 4.000000000000000000 ) ;
#11328=DIRECTION ( 'NONE',  ( -1.000000000000000000, -0.000000000000000000, -0.000000000000000000 ) ) ;
#11345=CARTESIAN_POINT ( 'NONE',  ( 4.700000000000000178, 5.629165124598848102, -3.250000000000007994 ) ) ;
#11369=FACE_OUTER_BOUND ( 'NONE', #19529, .T. ) ;
#11379=CARTESIAN_POINT ( 'NONE',  ( 5.299999999999999822, -7.505553499465150047, 0.000000000000000000 ) ) ;
#11406=EDGE_LOOP ( 'NONE', ( #9830, #4655, #1938, #321, #9283, #11459 ) ) ;
#11435=ORIENTED_EDGE ( 'NONE', *, *, #2847, .T. ) ;
#11449=DIRECTION ( 'NONE',  ( 0.000000000000000000, 0.000000000000000000, -1.000000000000000000 ) ) ;
#11459=ORIENTED_EDGE ( 'NONE', *, *, #6703, .F. ) ;
#11475=PLANE ( 'NONE',  #14312 ) ;
#11480=DIRECTION ( 'NONE',  ( -1.000000000000000000, -0.000000000000000000, -0.000000000000000000 ) ) ;
#11481=AXIS2_PLACEMENT_3D ( 'NONE', #20674, #14310, #20893 ) ;
#11530=ADVANCED_FACE ( 'NONE', ( #9147 ), #4399, .T. ) ;
#11550=VERTEX_POINT ( 'NONE', #20526 ) ;
#11723=DIRECTION ( 'NONE',  ( 1.000000000000000000, 0.000000000000000000, 0.000000000000000000 ) ) ;
#11748=CARTESIAN_POINT ( 'NONE',  ( 0.000000000000000000, 0.000000000000000000, 0.000000000000000000 ) ) ;
#11776=DIRECTION ( 'NONE',  ( -0.000000000000000000, 0.000000000000000000, 1.000000000000000000 ) ) ;
#11784=ORIENTED_EDGE ( 'NONE', *, *, #910, .T. ) ;
#11829=LINE ( 'NONE', #19839, #15572 ) ;
#11887=ORIENTED_EDGE ( 'NONE', *, *, #16114, .T. ) ;
#11897=VERTEX_POINT ( 'NONE', #5667 ) ;
#11903=CARTESIAN_POINT ( 'NONE',  ( 5.299999999999999822, 7.505553499465139389, 0.000000000000000000 ) ) ;
#11917=DIRECTION ( 'NONE',  ( 1.000000000000000000, 0.000000000000000000, 0.000000000000000000 ) ) ;
#11980=MANIFOLD_SOLID_BREP ( 'HeadFillet', #13145 ) ;
#11988=CIRCLE ( 'NONE', #963, 3.309499999999999886 ) ;
#12047=ORIENTED_EDGE ( 'NONE', *, *, #6260, .F. ) ;
#12053=DIRECTION ( 'NONE',  ( 0.000000000000000000, -1.000000000000000000, 0.000000000000000000 ) ) ;
#12133=FACE_OUTER_BOUND ( 'NONE', #18801, .T. ) ;
#12318=CIRCLE ( 'NONE', #18874, 6.500000000000000888 ) ;
#12389=CARTESIAN_POINT ( 'NONE',  ( 0.01372220897661874210, -5.309964801958117597, 3.802871176606137826 ) ) ;
#12399=VERTEX_POINT ( 'NONE', #3954 ) ;
#12402=ORIENTED_EDGE ( 'NONE', *, *, #6564, .F. ) ;
#12451=( GEOMETRIC_REPRESENTATION_CONTEXT ( 3 ) GLOBAL_UNCERTAINTY_ASSIGNED_CONTEXT ( ( #18926 ) ) GLOBAL_UNIT_ASSIGNED_CONTEXT ( ( #12998, #9636, #3869 ) ) REPRESENTATION_CONTEXT ( 'NONE', 'WORKASPACE' ) );
#12459=STYLED_ITEM('',(#21442),#11980);
#12480=CONICAL_SURFACE ( 'NONE', #16979, 6.500000000000000000, 1.047197551196600296 ) ;
#12492=LINE ( 'NONE', #2538, #13494 ) ;
#12527=DIRECTION ( 'NONE',  ( 0.000000000000000000, 0.000000000000000000, -1.000000000000000000 ) ) ;
#12534=CARTESIAN_POINT ( 'NONE',  ( 0.000000000000000000, 0.000000000000000000, 0.000000000000000000 ) ) ;
#12561=DIRECTION ( 'NONE',  ( 0.000000000000000000, 0.000000000000000000, 1.000000000000000000 ) ) ;
#12570=FACE_OUTER_BOUND ( 'NONE', #19856, .T. ) ;
#12574=FACE_OUTER_BOUND ( 'NONE', #10028, .T. ) ;
#12605=CARTESIAN_POINT ( 'NONE',  ( 21.30000000000000071, 4.475777889183788807E-16, -3.309499999999999886 ) ) ;
#12612=EDGE_CURVE ( 'NONE', #15843, #19525, #12900, .T. ) ;
#12650=ORIENTED_EDGE ( 'NONE', *, *, #12612, .F. ) ;
#12704=ORIENTED_EDGE ( 'NONE', *, *, #648, .F. ) ;
#12742=PLANE ( 'NONE',  #17494 ) ;
#12767=PLANE ( 'NONE',  #17646 ) ;
#12792=DIRECTION ( 'NONE',  ( 0.000000000000000000, 0.000000000000000000, -1.000000000000000000 ) ) ;
#12794=AXIS2_PLACEMENT_3D ( 'NONE', #808, #2419, #696 ) ;
#12838=VERTEX_POINT ( 'NONE', #1682 ) ;
#12858=CARTESIAN_POINT ( 'NONE',  ( 4.700000000000000178, 3.752776749732560368, -6.499999999999999112 ) ) ;
#12874=LINE ( 'NONE', #10811, #742 ) ;
#12900=B_SPLINE_CURVE_WITH_KNOTS ( 'NONE', 3,
 ( #20400, #18766, #12389, #17057, #20296, #5466, #2240, #4164 ),
 .UNSPECIFIED., .F., .F.,
 ( 4, 2, 2, 4 ),
 ( 0.003797433802554464090, 0.004743183970586256973, 0.005688934138618050723, 0.007580434474681636489 ),
 .UNSPECIFIED. ) ;
#12945=ORIENTED_EDGE ( 'NONE', *, *, #6703, .T. ) ;
#12984=VERTEX_POINT ( 'NONE', #3819 ) ;
#12998=( LENGTH_UNIT ( ) NAMED_UNIT ( * ) SI_UNIT ( .MILLI., .METRE. ) );
#13029=CARTESIAN_POINT ( 'NONE',  ( 20.60949999999999349, 0.000000000000000000, 0.000000000000000000 ) ) ;
#13062=FACE_OUTER_BOUND ( 'NONE', #1311, .T. ) ;
#13079=EDGE_CURVE ( 'NONE', #15843, #5613, #924, .T. ) ;
#13087=CIRCLE ( 'NONE', #19290, 6.500000000000000888 ) ;
#13091=ORIENTED_EDGE ( 'NONE', *, *, #2847, .F. ) ;
#13094=CARTESIAN_POINT ( 'NONE',  ( 0.5805565836007597902, 3.752776749732560368, -6.499999999999999112 ) ) ;
#13145=CLOSED_SHELL ( 'NONE', ( #5860, #9074, #13382, #338, #5918, #19214, #17161, #6001, #11530, #15312, #3749, #7038, #21298, #3277, #14413, #5470, #8687, #1178, #3546, #4917, #20072, #10754, #5614, #855, #5602, #17811, #19921, #15767, #3788 ) ) ;
#13153=CONICAL_SURFACE ( 'NONE', #19700, 6.500000000000000000, 1.047197551196600296 ) ;
#13200=CARTESIAN_POINT ( 'NONE',  ( 0.000000000000000000, 0.000000000000000000, 0.000000000000000000 ) ) ;
#13228=B_SPLINE_CURVE_WITH_KNOTS ( 'NONE', 3,
 ( #15068, #9959, #19697, #8225, #9744, #13335 ),
 .UNSPECIFIED., .F., .F.,
 ( 4, 2, 4 ),
 ( 0.01067228060976418286, 0.01257272967502433454, 0.01447317874028448623 ),
 .UNSPECIFIED. ) ;
#13253=CIRCLE ( 'NONE', #20502, 4.000000000000000000 ) ;
#13276=DIRECTION ( 'NONE',  ( 0.000000000000000000, 0.000000000000000000, 1.000000000000000000 ) ) ;
#13278=DIRECTION ( 'NONE',  ( 0.000000000000000000, 0.000000000000000000, 1.000000000000000000 ) ) ;
#13279=LINE ( 'NONE', #10220, #14616 ) ;
#13297=CARTESIAN_POINT ( 'NONE',  ( 21.30000000000000071, 0.000000000000000000, 0.000000000000000000 ) ) ;
#13331=EDGE_CURVE ( 'NONE', #10315, #18480, #20953, .T. ) ;
#13335=CARTESIAN_POINT ( 'NONE',  ( 0.5805565836007611225, 3.752776749732563477, 6.500000000000000000 ) ) ;
#13376=EDGE_LOOP ( 'NONE', ( #8020, #15261, #7887, #14233 ) ) ;
#13382=ADVANCED_FACE ( 'NONE', ( #11369 ), #579, .T. ) ;
#13404=CARTESIAN_POINT ( 'NONE',  ( 0.000000000000000000, 0.000000000000000000, 4.000000000000000000 ) ) ;
#13413=PLANE ( 'NONE',  #5213 ) ;
#13461=DIRECTION ( 'NONE',  ( -1.000000000000000000, -0.000000000000000000, -0.000000000000000000 ) ) ;
#13469=EDGE_CURVE ( 'NONE', #10793, #11897, #7111, .T. ) ;
#13494=VECTOR ( 'NONE', #12053, 1000.000000000000000 ) ;
#13551=CARTESIAN_POINT ( 'NONE',  ( 5.299999999999999822, 0.000000000000000000, -4.400000000000000355 ) ) ;
#13607=CARTESIAN_POINT ( 'NONE',  ( 21.30000000000000071, 0.000000000000000000, 3.309499999999999886 ) ) ;
#13633=VERTEX_POINT ( 'NONE', #20029 ) ;
#13678=EDGE_CURVE ( 'NONE', #15898, #8381, #9275, .T. ) ;
#13719=ORIENTED_EDGE ( 'NONE', *, *, #5844, .F. ) ;
#13815=DIRECTION ( 'NONE',  ( 0.000000000000000000, -0.5000000000000008882, 0.8660254037844381525 ) ) ;
#13843=VERTEX_POINT ( 'NONE', #16101 ) ;
#13857=EDGE_CURVE ( 'NONE', #6220, #13843, #10017, .T. ) ;
#13859=CIRCLE ( 'NONE', #4525, 4.400000000000000355 ) ;
#13909=VECTOR ( 'NONE', #21145, 1000.000000000000114 ) ;
#13936=CARTESIAN_POINT ( 'NONE',  ( 4.700000000000000178, 6.500000000000000888, 0.000000000000000000 ) ) ;
#13978=CARTESIAN_POINT ( 'NONE',  ( 21.30000000000000071, 0.000000000000000000, 0.000000000000000000 ) ) ;
#14008=CARTESIAN_POINT ( 'NONE',  ( 5.700000000000000178, 5.388445916248354013E-16, 4.400000000000000355 ) ) ;
#14022=CARTESIAN_POINT ( 'NONE',  ( 0.4033376246892473316, 4.059728990630800283, 5.968343123267133343 ) ) ;
#14026=CARTESIAN_POINT ( 'NONE',  ( 0.4037800551813700012, 4.058962678540093627, -5.969670414742686226 ) ) ;
#14036=ORIENTED_EDGE ( 'NONE', *, *, #5844, .T. ) ;
#14057=EDGE_CURVE ( 'NONE', #6373, #3963, #10441, .T. ) ;
#14081=DIRECTION ( 'NONE',  ( 0.000000000000000000, 0.000000000000000000, 1.000000000000000000 ) ) ;
#14130=CARTESIAN_POINT ( 'NONE',  ( 5.299999999999999822, -3.752776749732563033, 6.500000000000000000 ) ) ;
#14152=DIRECTION ( 'NONE',  ( 0.000000000000000000, 0.000000000000000000, -1.000000000000000000 ) ) ;
#14181=EDGE_CURVE ( 'NONE', #15214, #2614, #14563, .T. ) ;
#14233=ORIENTED_EDGE ( 'NONE', *, *, #16114, .F. ) ;
#14247=B_SPLINE_CURVE_WITH_KNOTS ( 'NONE', 3,
 ( #18789, #17397, #10670, #15460, #17186, #10563, #20856, #7534 ),
 .UNSPECIFIED., .F., .F.,
 ( 4, 2, 2, 4 ),
 ( 0.003797433802554437202, 0.004743183970586235289, 0.005688934138618033376, 0.007580434474681629550 ),
 .UNSPECIFIED. ) ;
#14310=DIRECTION ( 'NONE',  ( 1.000000000000000000, 0.000000000000000000, 0.000000000000000000 ) ) ;
#14312=AXIS2_PLACEMENT_3D ( 'NONE', #11903, #14741, #9740 ) ;
#14348=DIRECTION ( 'NONE',  ( 0.000000000000000000, 0.000000000000000000, -1.000000000000000000 ) ) ;
#14358=DIRECTION ( 'NONE',  ( -1.000000000000000000, -0.000000000000000000, -0.000000000000000000 ) ) ;
#14364=ORIENTED_EDGE ( 'NONE', *, *, #5380, .T. ) ;
#14372=CARTESIAN_POINT ( 'NONE',  ( 0.05533025579362074037, 6.264553569211843254, -2.149474931388136500 ) ) ;
#14413=ADVANCED_FACE ( 'NONE', ( #5132 ), #1576, .T. ) ;
#14414=ORIENTED_EDGE ( 'NONE', *, *, #8363, .T. ) ;
#14445=( NAMED_UNIT ( * ) SI_UNIT ( $, .STERADIAN. ) SOLID_ANGLE_UNIT ( ) );
#14453=CARTESIAN_POINT ( 'NONE',  ( 0.000000000000000000, -5.629165124598848990, -3.250000000000004441 ) ) ;
#14462=ORIENTED_EDGE ( 'NONE', *, *, #10448, .T. ) ;
#14491=AXIS2_PLACEMENT_3D ( 'NONE', #7264, #2311, #8678 ) ;
#14506=DIRECTION ( 'NONE',  ( 1.000000000000000000, 0.000000000000000000, 0.000000000000000000 ) ) ;
#14563=LINE ( 'NONE', #19625, #10246 ) ;
#14605=TOROIDAL_SURFACE ( 'NONE', #19422, 4.400000000000000355, 0.4000000000000000222 ) ;
#14612=EDGE_CURVE ( 'NONE', #4925, #10315, #6435, .T. ) ;
#14616=VECTOR ( 'NONE', #20086, 1000.000000000000000 ) ;
#14677=EDGE_LOOP ( 'NONE', ( #7625, #7763, #13719, #13091 ) ) ;
#14683=ORIENTED_EDGE ( 'NONE', *, *, #3281, .T. ) ;
#14697=CARTESIAN_POINT ( 'NONE',  ( 5.299999999999999822, 3.752776749732563033, 6.500000000000000000 ) ) ;
#14705=EDGE_LOOP ( 'NONE', ( #14364, #21045, #2146 ) ) ;
#14741=DIRECTION ( 'NONE',  ( 0.000000000000000000, -0.8660254037844381525, -0.5000000000000008882 ) ) ;
#14747=DIRECTION ( 'NONE',  ( 0.000000000000000000, 0.000000000000000000, 1.000000000000000000 ) ) ;
#14768=LINE ( 'NONE', #8137, #18394 ) ;
#14779=ORIENTED_EDGE ( 'NONE', *, *, #5872, .T. ) ;
#14840=EDGE_CURVE ( 'NONE', #10793, #2403, #18450, .T. ) ;
#14845=APPLICATION_CONTEXT ( 'automotive_design' ) ;
#14855=DIRECTION ( 'NONE',  ( -1.000000000000000000, -0.000000000000000000, -0.000000000000000000 ) ) ;
#14876=CARTESIAN_POINT ( 'NONE',  ( 4.700000000000000178, 6.500000000000000888, 0.000000000000000000 ) ) ;
#14881=CARTESIAN_POINT ( 'NONE',  ( 0.000000000000000000, 0.000000000000000000, 0.000000000000000000 ) ) ;
#14904=AXIS2_PLACEMENT_3D ( 'NONE', #1035, #19292, #16063 ) ;
#14930=CARTESIAN_POINT ( 'NONE',  ( 5.299999999999999822, 3.752776749732560368, -6.499999999999999112 ) ) ;
#14966=ORIENTED_EDGE ( 'NONE', *, *, #19532, .T. ) ;
#14984=CARTESIAN_POINT ( 'NONE',  ( 4.700000000000000178, 6.500000000000000888, 0.000000000000000000 ) ) ;
#15022=DIRECTION ( 'NONE',  ( -0.7071067811865511255, 0.000000000000000000, 0.7071067811865440200 ) ) ;
#15033=CARTESIAN_POINT ( 'NONE',  ( 0.5805565836007715586, -7.505553499465150935, -4.964436717930768604E-16 ) ) ;
#15068=CARTESIAN_POINT ( 'NONE',  ( 0.000000000000000000, 0.000000000000000000, 6.500000000000000000 ) ) ;
#15093=CARTESIAN_POINT ( 'NONE',  ( 0.000000000000000000, 0.000000000000000000, 0.000000000000000000 ) ) ;
#15099=DIRECTION ( 'NONE',  ( -1.000000000000000000, -0.000000000000000000, -0.000000000000000000 ) ) ;
#15105=ORIENTED_EDGE ( 'NONE', *, *, #14612, .F. ) ;
#15156=EDGE_LOOP ( 'NONE', ( #18161, #19660, #15589, #1742, #794, #3858 ) ) ;
#15165=DIRECTION ( 'NONE',  ( 1.000000000000000000, 0.000000000000000000, -0.000000000000000000 ) ) ;
#15190=PRODUCT_CONTEXT ( 'NONE', #887, 'mechanical' ) ;
#15197=PLANE ( 'NONE',  #8983 ) ;
#15214=VERTEX_POINT ( 'NONE', #7924 ) ;
#15234=AXIS2_PLACEMENT_3D ( 'NONE', #19672, #8420, #1625 ) ;
#15261=ORIENTED_EDGE ( 'NONE', *, *, #648, .T. ) ;
#15286=ORIENTED_EDGE ( 'NONE', *, *, #12612, .T. ) ;
#15308=DIRECTION ( 'NONE',  ( -1.000000000000000000, -0.000000000000000000, -0.000000000000000000 ) ) ;
#15312=ADVANCED_FACE ( 'NONE', ( #18204 ), #1676, .T. ) ;
#15423=( LENGTH_UNIT ( ) NAMED_UNIT ( * ) SI_UNIT ( .MILLI., .METRE. ) );
#15460=CARTESIAN_POINT ( 'NONE',  ( 0.06682554136337878758, 6.264794173742276762, 2.149058192116893640 ) ) ;
#15472=ORIENTED_EDGE ( 'NONE', *, *, #774, .T. ) ;
#15487=CARTESIAN_POINT ( 'NONE',  ( 0.000000000000000000, 7.505553499465139389, 0.000000000000000000 ) ) ;
#15491=ORIENTED_EDGE ( 'NONE', *, *, #9827, .T. ) ;
#15518=DIRECTION ( 'NONE',  ( 0.000000000000000000, 1.224646799147353207E-16, 1.000000000000000000 ) ) ;
#15523=ORIENTED_EDGE ( 'NONE', *, *, #19803, .F. ) ;
#15572=VECTOR ( 'NONE', #13461, 1000.000000000000000 ) ;
#15589=ORIENTED_EDGE ( 'NONE', *, *, #4453, .F. ) ;
#15623=CARTESIAN_POINT ( 'NONE',  ( 4.700000000000000178, 0.000000000000000000, 0.000000000000000000 ) ) ;
#15649=LINE ( 'NONE', #14130, #6638 ) ;
#15654=AXIS2_PLACEMENT_3D ( 'NONE', #21167, #4823, #11213 ) ;
#15748=CARTESIAN_POINT ( 'NONE',  ( 0.05533025579362052526, 4.993776679985852951, 4.350525068611870161 ) ) ;
#15767=ADVANCED_FACE ( 'NONE', ( #18148 ), #6684, .F. ) ;
#15768=ORIENTED_EDGE ( 'NONE', *, *, #20375, .F. ) ;
#15820=DIRECTION ( 'NONE',  ( -1.000000000000000000, -0.000000000000000000, -0.000000000000000000 ) ) ;
#15843=VERTEX_POINT ( 'NONE', #4279 ) ;
#15890=DIRECTION ( 'NONE',  ( 0.000000000000000000, 0.000000000000000000, -1.000000000000000000 ) ) ;
#15891=CARTESIAN_POINT ( 'NONE',  ( 4.700000000000000178, -7.505553499465150047, 0.000000000000000000 ) ) ;
#15898=VERTEX_POINT ( 'NONE', #10755 ) ;
#15920=ORIENTED_EDGE ( 'NONE', *, *, #481, .T. ) ;
#15927=AXIS2_PLACEMENT_3D ( 'NONE', #17974, #3175, #16378 ) ;
#15964=CARTESIAN_POINT ( 'NONE',  ( 2.112500170452225440E-15, -5.309483803148807191, -3.803704290982254932 ) ) ;
#16014=ORIENTED_EDGE ( 'NONE', *, *, #4938, .T. ) ;
#16024=CARTESIAN_POINT ( 'NONE',  ( 5.299999999999999822, 3.752776749732560368, -6.499999999999999112 ) ) ;
#16028=ORIENTED_EDGE ( 'NONE', *, *, #4938, .F. ) ;
#16035=LINE ( 'NONE', #17748, #20372 ) ;
#16037=CIRCLE ( 'NONE', #6687, 6.500000000000000888 ) ;
#16057=ORIENTED_EDGE ( 'NONE', *, *, #4665, .F. ) ;
#16059=ORIENTED_EDGE ( 'NONE', *, *, #5592, .T. ) ;
#16063=DIRECTION ( 'NONE',  ( 0.000000000000000000, 0.000000000000000000, 1.000000000000000000 ) ) ;
#16071=CARTESIAN_POINT ( 'NONE',  ( 0.5805565836007642311, -3.752776749732576356, -6.499999999999999112 ) ) ;
#16101=CARTESIAN_POINT ( 'NONE',  ( 20.60949999999999349, 0.000000000000000000, 4.000000000000000000 ) ) ;
#16108=DIRECTION ( 'NONE',  ( -0.000000000000000000, 0.5000000000000011102, 0.8660254037844379305 ) ) ;
#16114=EDGE_CURVE ( 'NONE', #12838, #13843, #7131, .T. ) ;
#16186=ORIENTED_EDGE ( 'NONE', *, *, #5592, .F. ) ;
#16232=FACE_OUTER_BOUND ( 'NONE', #8346, .T. ) ;
#16317=DIRECTION ( 'NONE',  ( 0.000000000000000000, 0.000000000000000000, -1.000000000000000000 ) ) ;
#16334=B_SPLINE_CURVE_WITH_KNOTS ( 'NONE', 3,
 ( #9480, #4616, #5804, #20630, #20852, #7745 ),
 .UNSPECIFIED., .F., .F.,
 ( 4, 2, 4 ),
 ( 0.006874058788776910706, 0.008773169699270546781, 0.01067228060976418286 ),
 .UNSPECIFIED. ) ;
#16378=DIRECTION ( 'NONE',  ( 0.000000000000000000, 0.000000000000000000, -1.000000000000000000 ) ) ;
#16469=VECTOR ( 'NONE', #3167, 1000.000000000000227 ) ;
#16470=LINE ( 'NONE', #17962, #1646 ) ;
#16481=VECTOR ( 'NONE', #13815, 1000.000000000000000 ) ;
#16496=CARTESIAN_POINT ( 'NONE',  ( 5.700000000000000178, 4.898587196589412829E-16, -4.000000000000000000 ) ) ;
#16525=CARTESIAN_POINT ( 'NONE',  ( 0.2565376335220210802, -2.516992571281988056, -6.499999999999999112 ) ) ;
#16555=CARTESIAN_POINT ( 'NONE',  ( 4.700000000000000178, 3.752776749732560368, -6.499999999999999112 ) ) ;
#16562=CARTESIAN_POINT ( 'NONE',  ( 4.700000000000000178, 3.752776749732563033, 6.500000000000000000 ) ) ;
#16570=AXIS2_PLACEMENT_3D ( 'NONE', #18705, #15165, #3891 ) ;
#16695=EDGE_CURVE ( 'NONE', #2403, #18883, #16470, .T. ) ;
#16710=DIRECTION ( 'NONE',  ( 0.000000000000000000, 0.000000000000000000, -1.000000000000000000 ) ) ;
#16835=ORIENTED_EDGE ( 'NONE', *, *, #13079, .T. ) ;
#16915=SHAPE_DEFINITION_REPRESENTATION ( #8199, #4076 ) ;
#16960=AXIS2_PLACEMENT_3D ( 'NONE', #13936, #18887, #959 ) ;
#16979=AXIS2_PLACEMENT_3D ( 'NONE', #14881, #6633, #19843 ) ;
#17057=CARTESIAN_POINT ( 'NONE',  ( 0.06682554136338046680, -4.993536075455419443, 4.350941807883118351 ) ) ;
#17110=CARTESIAN_POINT ( 'NONE',  ( 4.700000000000000178, -3.752776749732576800, -6.499999999999999112 ) ) ;
#17161=ADVANCED_FACE ( 'NONE', ( #7453 ), #9581, .T. ) ;
#17186=CARTESIAN_POINT ( 'NONE',  ( 0.1061556211655339810, 6.421950209808280796, 1.876855952934450622 ) ) ;
#17226=EDGE_CURVE ( 'NONE', #6220, #8661, #11988, .T. ) ;
#17238=DIRECTION ( 'NONE',  ( 0.000000000000000000, -0.5000000000000008882, 0.8660254037844381525 ) ) ;
#17245=CONICAL_SURFACE ( 'NONE', #17579, 6.500000000000000000, 1.047197551196600296 ) ;
#17261=CARTESIAN_POINT ( 'NONE',  ( 0.5805565836007597902, 3.752776749732560368, -6.499999999999999112 ) ) ;
#17311=AXIS2_PLACEMENT_3D ( 'NONE', #13200, #1516, #11449 ) ;
#17397=CARTESIAN_POINT ( 'NONE',  ( -3.905386575473828482E-15, 5.788408252967903067, 2.974182810908597041 ) ) ;
#17466=DIRECTION ( 'NONE',  ( -1.000000000000000000, -0.000000000000000000, -0.000000000000000000 ) ) ;
#17494=AXIS2_PLACEMENT_3D ( 'NONE', #14697, #16317, #17916 ) ;
#17534=ORIENTED_EDGE ( 'NONE', *, *, #910, .F. ) ;
#17539=DIRECTION ( 'NONE',  ( -0.000000000000000000, 0.8660254037844382635, 0.5000000000000008882 ) ) ;
#17579=AXIS2_PLACEMENT_3D ( 'NONE', #10964, #2442, #14348 ) ;
#17645=PLANE ( 'NONE',  #7280 ) ;
#17646=AXIS2_PLACEMENT_3D ( 'NONE', #16024, #21089, #14506 ) ;
#17691=ORIENTED_EDGE ( 'NONE', *, *, #8363, .F. ) ;
#17736=EDGE_CURVE ( 'NONE', #21185, #15843, #12318, .T. ) ;
#17748=CARTESIAN_POINT ( 'NONE',  ( 21.30000000000000071, 4.052968581778165278E-16, -3.309499999999999886 ) ) ;
#17763=DIRECTION ( 'NONE',  ( -1.000000000000000000, -0.000000000000000000, 0.000000000000000000 ) ) ;
#17782=EDGE_CURVE ( 'NONE', #18587, #13633, #1278, .T. ) ;
#17811=ADVANCED_FACE ( 'NONE', ( #13062 ), #12742, .F. ) ;
#17916=DIRECTION ( 'NONE',  ( -1.000000000000000000, 0.000000000000000000, -0.000000000000000000 ) ) ;
#17940=DIRECTION ( 'NONE',  ( -1.000000000000000000, -0.000000000000000000, 0.000000000000000000 ) ) ;
#17962=CARTESIAN_POINT ( 'NONE',  ( 4.700000000000000178, 3.752776749732560368, -6.499999999999999112 ) ) ;
#17974=CARTESIAN_POINT ( 'NONE',  ( 0.000000000000000000, 0.000000000000000000, 0.000000000000000000 ) ) ;
#17976=DIRECTION ( 'NONE',  ( -1.000000000000000000, -0.000000000000000000, -0.000000000000000000 ) ) ;
#17981=( NAMED_UNIT ( * ) PLANE_ANGLE_UNIT ( ) SI_UNIT ( $, .RADIAN. ) );
#17997=CIRCLE ( 'NONE', #9369, 6.500000000000000888 ) ;
#18060=ORIENTED_EDGE ( 'NONE', *, *, #5380, .F. ) ;
#18089=ORIENTED_EDGE ( 'NONE', *, *, #3737, .F. ) ;
#18103=CONICAL_SURFACE ( 'NONE', #8774, 6.500000000000000000, 1.047197551196600296 ) ;
#18121=CARTESIAN_POINT ( 'NONE',  ( 0.000000000000000000, 5.629165124598846326, -3.250000000000007550 ) ) ;
#18148=FACE_OUTER_BOUND ( 'NONE', #11406, .T. ) ;
#18161=ORIENTED_EDGE ( 'NONE', *, *, #5872, .F. ) ;
#18178=FACE_OUTER_BOUND ( 'NONE', #18335, .T. ) ;
#18192=DIRECTION ( 'NONE',  ( 1.000000000000000000, 0.000000000000000000, 0.000000000000000000 ) ) ;
#18204=FACE_OUTER_BOUND ( 'NONE', #9168, .T. ) ;
#18269=ORIENTED_EDGE ( 'NONE', *, *, #6260, .T. ) ;
#18276=EDGE_CURVE ( 'NONE', #8381, #11550, #19816, .T. ) ;
#18293=CARTESIAN_POINT ( 'NONE',  ( 4.700000000000000178, -7.505553499465150047, 0.000000000000000000 ) ) ;
#18315=DIRECTION ( 'NONE',  ( 0.000000000000000000, 0.000000000000000000, -1.000000000000000000 ) ) ;
#18322=CARTESIAN_POINT ( 'NONE',  ( 0.000000000000000000, 0.000000000000000000, 0.000000000000000000 ) ) ;
#18330=ORIENTED_EDGE ( 'NONE', *, *, #19661, .F. ) ;
#18335=EDGE_LOOP ( 'NONE', ( #16028, #4971, #8432, #1109, #12047, #8702 ) ) ;
#18373=DIRECTION ( 'NONE',  ( 1.000000000000000000, 0.000000000000000000, -0.000000000000000000 ) ) ;
#18386=ORIENTED_EDGE ( 'NONE', *, *, #18276, .F. ) ;
#18394=VECTOR ( 'NONE', #5999, 1000.000000000000000 ) ;
#18450=LINE ( 'NONE', #3635, #6450 ) ;
#18480=VERTEX_POINT ( 'NONE', #13551 ) ;
#18483=DIRECTION ( 'NONE',  ( 0.000000000000000000, 0.000000000000000000, 1.000000000000000000 ) ) ;
#18511=CARTESIAN_POINT ( 'NONE',  ( 0.000000000000000000, 0.000000000000000000, 0.000000000000000000 ) ) ;
#18527=FACE_OUTER_BOUND ( 'NONE', #19164, .T. ) ;
#18555=CARTESIAN_POINT ( 'NONE',  ( -4.764560328305437435E-16, -0.6346842323199950453, -6.500000000000000000 ) ) ;
#18586=ORIENTED_EDGE ( 'NONE', *, *, #20375, .T. ) ;
#18587=VERTEX_POINT ( 'NONE', #17110 ) ;
#18668=AXIS2_PLACEMENT_3D ( 'NONE', #8088, #18373, #5071 ) ;
#18686=VECTOR ( 'NONE', #17238, 1000.000000000000000 ) ;
#18697=DIRECTION ( 'NONE',  ( 1.000000000000000000, 0.000000000000000000, 0.000000000000000000 ) ) ;
#18705=CARTESIAN_POINT ( 'NONE',  ( 5.700000000000000178, 0.000000000000000000, 0.000000000000000000 ) ) ;
#18766=CARTESIAN_POINT ( 'NONE',  ( -1.052014920489841021E-15, -5.469921996229796690, 3.525817189091422943 ) ) ;
#18777=CIRCLE ( 'NONE', #19148, 0.4000000000000001887 ) ;
#18789=CARTESIAN_POINT ( 'NONE',  ( 0.000000000000000000, 5.629165124598848102, 3.250000000000005329 ) ) ;
#18801=EDGE_LOOP ( 'NONE', ( #7019, #9282, #15286 ) ) ;
#18860=CARTESIAN_POINT ( 'NONE',  ( 0.2573354458087815932, 4.368923434677189022, 5.432802636760778014 ) ) ;
#18869=DIRECTION ( 'NONE',  ( 0.000000000000000000, -0.8660254037844380415, 0.5000000000000012212 ) ) ;
#18874=AXIS2_PLACEMENT_3D ( 'NONE', #12534, #2690, #15890 ) ;
#18883=VERTEX_POINT ( 'NONE', #11345 ) ;
#18887=DIRECTION ( 'NONE',  ( 1.000000000000000000, 0.000000000000000000, 0.000000000000000000 ) ) ;
#18926=UNCERTAINTY_MEASURE_WITH_UNIT (LENGTH_MEASURE( 1.000000000000000082E-05 ), #12998, 'distance_accuracy_value', 'NONE');
#18974=CARTESIAN_POINT ( 'NONE',  ( 0.5805565836007611225, 3.752776749732563477, 6.500000000000000000 ) ) ;
#18978=CARTESIAN_POINT ( 'NONE',  ( 0.2573354458087861452, -4.368923434677201456, -5.432802636760778903 ) ) ;
#19023=ORIENTED_EDGE ( 'NONE', *, *, #19589, .F. ) ;
#19077=VERTEX_POINT ( 'NONE', #2682 ) ;
#19145=EDGE_LOOP ( 'NONE', ( #3525, #6421, #4395 ) ) ;
#19148=AXIS2_PLACEMENT_3D ( 'NONE', #1074, #10992, #9379 ) ;
#19164=EDGE_LOOP ( 'NONE', ( #15472, #16835, #1373 ) ) ;
#19168=CARTESIAN_POINT ( 'NONE',  ( 0.05533025579362401553, -6.264553569211847694, 2.149474931388141385 ) ) ;
#19214=ADVANCED_FACE ( 'NONE', ( #5151 ), #8164, .T. ) ;
#19215=ORIENTED_EDGE ( 'NONE', *, *, #21057, .F. ) ;
#19218=ORIENTED_EDGE ( 'NONE', *, *, #6116, .F. ) ;
#19220=CARTESIAN_POINT ( 'NONE',  ( 0.000000000000000000, 0.000000000000000000, 0.000000000000000000 ) ) ;
#19221=AXIS2_PLACEMENT_3D ( 'NONE', #3479, #14855, #14747 ) ;
#19237=AXIS2_PLACEMENT_3D ( 'NONE', #13029, #19620, #4798 ) ;
#19269=CARTESIAN_POINT ( 'NONE',  ( 0.2573354458087876995, -6.889406814520521394, 1.067197363239227537 ) ) ;
#19290=AXIS2_PLACEMENT_3D ( 'NONE', #8059, #9898, #13276 ) ;
#19292=DIRECTION ( 'NONE',  ( -1.000000000000000000, -0.000000000000000000, -0.000000000000000000 ) ) ;
#19317=EDGE_LOOP ( 'NONE', ( #19629, #151, #19792 ) ) ;
#19422=AXIS2_PLACEMENT_3D ( 'NONE', #10822, #2615, #7784 ) ;
#19461=CIRCLE ( 'NONE', #20864, 6.500000000000000888 ) ;
#19501=ORIENTED_EDGE ( 'NONE', *, *, #20722, .T. ) ;
#19525=VERTEX_POINT ( 'NONE', #10752 ) ;
#19529=EDGE_LOOP ( 'NONE', ( #7809, #14462, #8905, #5661 ) ) ;
#19532=EDGE_CURVE ( 'NONE', #5342, #12984, #8170, .T. ) ;
#19589=EDGE_CURVE ( 'NONE', #13633, #5613, #21093, .T. ) ;
#19620=DIRECTION ( 'NONE',  ( -1.000000000000000000, -0.000000000000000000, -0.000000000000000000 ) ) ;
#19625=CARTESIAN_POINT ( 'NONE',  ( 5.299999999999999822, 7.505553499465139389, 0.000000000000000000 ) ) ;
#19629=ORIENTED_EDGE ( 'NONE', *, *, #19589, .T. ) ;
#19660=ORIENTED_EDGE ( 'NONE', *, *, #17782, .T. ) ;
#19661=EDGE_CURVE ( 'NONE', #3061, #8258, #20508, .T. ) ;
#19672=CARTESIAN_POINT ( 'NONE',  ( 5.299999999999999822, 7.505553499465139389, 0.000000000000000000 ) ) ;
#19697=CARTESIAN_POINT ( 'NONE',  ( 0.05613245601076820995, 1.278525034532179250, 6.500000000000002665 ) ) ;
#19698=DIRECTION ( 'NONE',  ( 0.000000000000000000, 0.000000000000000000, 1.000000000000000000 ) ) ;
#19700=AXIS2_PLACEMENT_3D ( 'NONE', #15093, #171, #6846 ) ;
#19742=CONICAL_SURFACE ( 'NONE', #771, 6.500000000000000000, 1.047197551196600296 ) ;
#19747=CARTESIAN_POINT ( 'NONE',  ( 0.4033376246892498296, 7.198601258566900363, -0.5316568767328675449 ) ) ;
#19792=ORIENTED_EDGE ( 'NONE', *, *, #4453, .T. ) ;
#19803=EDGE_CURVE ( 'NONE', #2116, #6373, #19461, .T. ) ;
#19816=LINE ( 'NONE', #18293, #16469 ) ;
#19826=ORIENTED_EDGE ( 'NONE', *, *, #14057, .T. ) ;
#19839=CARTESIAN_POINT ( 'NONE',  ( 0.000000000000000000, 7.960204194457796463E-16, -6.500000000000000888 ) ) ;
#19840=VECTOR ( 'NONE', #17976, 1000.000000000000000 ) ;
#19843=DIRECTION ( 'NONE',  ( 0.000000000000000000, 0.000000000000000000, -1.000000000000000000 ) ) ;
#19856=EDGE_LOOP ( 'NONE', ( #19826, #1193, #3630 ) ) ;
#19882=CARTESIAN_POINT ( 'NONE',  ( 0.01372220897662236594, -5.948365447239591042, -2.697128823393882158 ) ) ;
#19893=DIRECTION ( 'NONE',  ( 0.000000000000000000, 1.000000000000000000, -0.000000000000000000 ) ) ;
#19920=B_SPLINE_CURVE_WITH_KNOTS ( 'NONE', 3,
 ( #13094, #6802, #8531, #8635, #340, #9829 ),
 .UNSPECIFIED., .F., .F.,
 ( 4, 2, 4 ),
 ( 0.01913986446825127058, 0.02104055318008570680, 0.02294124189192014301 ),
 .UNSPECIFIED. ) ;
#19921=ADVANCED_FACE ( 'NONE', ( #18178 ), #11475, .F. ) ;
#19991=CARTESIAN_POINT ( 'NONE',  ( 0.06682554136338486606, -6.264794173742287420, -2.149058192116898081 ) ) ;
#20002=LINE ( 'NONE', #9719, #7272 ) ;
#20029=CARTESIAN_POINT ( 'NONE',  ( 0.5805565836007642311, -3.752776749732576356, -6.499999999999999112 ) ) ;
#20037=CARTESIAN_POINT ( 'NONE',  ( 21.30000000000000071, 0.000000000000000000, 3.309499999999999886 ) ) ;
#20051=CYLINDRICAL_SURFACE ( 'NONE', #14491, 6.500000000000000888 ) ;
#20061=CIRCLE ( 'NONE', #15927, 6.500000000000000888 ) ;
#20072=ADVANCED_FACE ( 'NONE', ( #8469 ), #13153, .T. ) ;
#20086=DIRECTION ( 'NONE',  ( -1.000000000000000000, -0.000000000000000000, -0.000000000000000000 ) ) ;
#20087=CARTESIAN_POINT ( 'NONE',  ( 0.000000000000000000, 0.000000000000000000, -6.499999999999999112 ) ) ;
#20102=ORIENTED_EDGE ( 'NONE', *, *, #6116, .T. ) ;
#20103=CARTESIAN_POINT ( 'NONE',  ( 0.2578475836320768821, -6.890627091270383531, -1.065083781909174743 ) ) ;
#20148=EDGE_LOOP ( 'NONE', ( #15768, #5499, #9750, #17691, #15523, #4261 ) ) ;
#20237=DIRECTION ( 'NONE',  ( -0.000000000000000000, 0.000000000000000000, -1.000000000000000000 ) ) ;
#20253=AXIS2_PLACEMENT_3D ( 'NONE', #1656, #11480, #19698 ) ;
#20296=CARTESIAN_POINT ( 'NONE',  ( 0.1061556211655353132, -4.836380039389418073, 4.623144047065560258 ) ) ;
#20372=VECTOR ( 'NONE', #2939, 1000.000000000000000 ) ;
#20375=EDGE_CURVE ( 'NONE', #8258, #3061, #9408, .T. ) ;
#20400=CARTESIAN_POINT ( 'NONE',  ( 0.000000000000000000, -5.629165124598843661, 3.250000000000012434 ) ) ;
#20502=AXIS2_PLACEMENT_3D ( 'NONE', #1088, #11328, #9598 ) ;
#20504=DIRECTION ( 'NONE',  ( -1.000000000000000000, -0.000000000000000000, -0.000000000000000000 ) ) ;
#20508=CIRCLE ( 'NONE', #11164, 6.500000000000000888 ) ;
#20516=CARTESIAN_POINT ( 'NONE',  ( 4.700000000000000178, 7.505553499465139389, 0.000000000000000000 ) ) ;
#20525=ORIENTED_EDGE ( 'NONE', *, *, #13079, .F. ) ;
#20526=CARTESIAN_POINT ( 'NONE',  ( 4.700000000000000178, -7.505553499465150047, 0.000000000000000000 ) ) ;
#20630=CARTESIAN_POINT ( 'NONE',  ( 0.05458999538792619344, -1.264741368075137817, 6.499999999999999112 ) ) ;
#20665=FACE_OUTER_BOUND ( 'NONE', #15156, .T. ) ;
#20671=CARTESIAN_POINT ( 'NONE',  ( 4.700000000000000178, 5.629165124598848102, 3.250000000000005773 ) ) ;
#20674=CARTESIAN_POINT ( 'NONE',  ( 4.700000000000000178, 6.500000000000000888, 0.000000000000000000 ) ) ;
#20722=EDGE_CURVE ( 'NONE', #3061, #2116, #13279, .T. ) ;
#20755=TOROIDAL_SURFACE ( 'NONE', #18668, 4.400000000000000355, 0.4000000000000000222 ) ;
#20816=EDGE_CURVE ( 'NONE', #15898, #19525, #15649, .T. ) ;
#20852=CARTESIAN_POINT ( 'NONE',  ( 1.863472483959460130E-17, -0.6346842323199924918, 6.499999999999999112 ) ) ;
#20856=CARTESIAN_POINT ( 'NONE',  ( 0.4037800551813739425, 7.199367570657606130, 0.5303295852573159941 ) ) ;
#20864=AXIS2_PLACEMENT_3D ( 'NONE', #8136, #21140, #21353 ) ;
#20884=DIRECTION ( 'NONE',  ( 0.000000000000000000, 0.5000000000000018874, 0.8660254037844375974 ) ) ;
#20893=DIRECTION ( 'NONE',  ( 0.000000000000000000, 0.000000000000000000, -1.000000000000000000 ) ) ;
#20927=FACE_OUTER_BOUND ( 'NONE', #1550, .T. ) ;
#20953=CIRCLE ( 'NONE', #21280, 4.400000000000000355 ) ;
#21002=CARTESIAN_POINT ( 'NONE',  ( 0.5805565836007715586, -7.505553499465150935, -4.964436717930768604E-16 ) ) ;
#21033=CARTESIAN_POINT ( 'NONE',  ( -5.055092629213673101E-15, 5.469921996229795802, -3.525817189091416282 ) ) ;
#21045=ORIENTED_EDGE ( 'NONE', *, *, #1652, .T. ) ;
#21057=EDGE_CURVE ( 'NONE', #2116, #15898, #14768, .T. ) ;
#21078=VERTEX_POINT ( 'NONE', #9458 ) ;
#21089=DIRECTION ( 'NONE',  ( -0.000000000000000000, 0.000000000000000000, 1.000000000000000000 ) ) ;
#21093=B_SPLINE_CURVE_WITH_KNOTS ( 'NONE', 3,
 ( #16071, #5780, #18978, #6096, #15964, #14453 ),
 .UNSPECIFIED., .F., .F.,
 ( 4, 2, 4 ),
 ( 2.380733003139562229E-07, 0.001898835937927372463, 0.003797433802554430696 ),
 .UNSPECIFIED. ) ;
#21104=CIRCLE ( 'NONE', #17311, 6.500000000000000888 ) ;
#21140=DIRECTION ( 'NONE',  ( -1.000000000000000000, -0.000000000000000000, -0.000000000000000000 ) ) ;
#21145=DIRECTION ( 'NONE',  ( 0.000000000000000000, 0.5000000000000007772, -0.8660254037844381525 ) ) ;
#21164=CARTESIAN_POINT ( 'NONE',  ( 4.700000000000000178, -5.629165124598843661, 3.250000000000012879 ) ) ;
#21167=CARTESIAN_POINT ( 'NONE',  ( 5.299999999999999822, 0.000000000000000000, 0.000000000000000000 ) ) ;
#21185=VERTEX_POINT ( 'NONE', #9661 ) ;
#21198=CARTESIAN_POINT ( 'NONE',  ( 21.30000000000000071, 0.000000000000000000, 0.000000000000000000 ) ) ;
#21202=EDGE_CURVE ( 'NONE', #8258, #10793, #11829, .T. ) ;
#21235=DIRECTION ( 'NONE',  ( 0.000000000000000000, 0.000000000000000000, -1.000000000000000000 ) ) ;
#21256=ORIENTED_EDGE ( 'NONE', *, *, #4061, .T. ) ;
#21280=AXIS2_PLACEMENT_3D ( 'NONE', #9432, #17763, #1331 ) ;
#21297=FACE_OUTER_BOUND ( 'NONE', #2067, .T. ) ;
#21298=ADVANCED_FACE ( 'NONE', ( #1793 ), #15197, .T. ) ;
#21300=AXIS2_PLACEMENT_3D ( 'NONE', #14930, #18869, #7613 ) ;
#21302=UNCERTAINTY_MEASURE_WITH_UNIT (LENGTH_MEASURE( 1.000000000000000082E-05 ), #15423, 'distance_accuracy_value', 'NONE');
#21308=VERTEX_POINT ( 'NONE', #16496 ) ;
#21353=DIRECTION ( 'NONE',  ( 0.000000000000000000, 0.000000000000000000, 1.000000000000000000 ) ) ;
#21436=COLOUR_RGB('Black',0.12,0.14,0.17);
#21437=FILL_AREA_STYLE_COLOUR('',#21436);
#21438=FILL_AREA_STYLE('',(#21437));
#21439=SURFACE_STYLE_FILL_AREA(#21438);
#21440=SURFACE_SIDE_STYLE('',(#21439));
#21441=SURFACE_STYLE_USAGE(.BOTH.,#21440);
#21442=PRESENTATION_STYLE_ASSIGNMENT((#21441));
ENDSEC;
END-ISO-10303-21;
